ISO-10303-21;
HEADER;
/* Generated by software containing ST-Developer
 * from STEP Tools, Inc. (www.steptools.com) 
 */

FILE_DESCRIPTION(
/* description */ ('Cable chain and bracket set'),
/* implementation_level */ '2;1');

FILE_NAME(
/* name */ 'Flat Washer - M6.step',
/* time_stamp */ '2026-10-29T17:19:47-07:00',
/* author */ (''),
/* organization */ (''),
/* preprocessor_version */ 'ST-DEVELOPER v20.2',
/* originating_system */ 'Autodesk Translation Framework v15.17.0.0',
/* authorisation */ '');

FILE_SCHEMA (('AUTOMOTIVE_DESIGN { 1 0 10303 214 3 1 1 }'));
ENDSEC;

DATA;
#10=MECHANICAL_DESIGN_GEOMETRIC_PRESENTATION_REPRESENTATION('',(#348),#5929);
#322=SHAPE_REPRESENTATION_RELATIONSHIP('SRR','None',#6060,#335);
#335=ADVANCED_BREP_SHAPE_REPRESENTATION('',(#361),#5927);
#348=STYLED_ITEM('',(#6227),#361);
#361=MANIFOLD_SOLID_BREP('Body1',#3342);
#401=FACE_BOUND('',#917,.T.);
#402=FACE_BOUND('',#919,.T.);
#517=PLANE('',#3744);
#518=PLANE('',#3745);
#694=FACE_OUTER_BOUND('',#914,.T.);
#695=FACE_OUTER_BOUND('',#915,.T.);
#696=FACE_OUTER_BOUND('',#916,.T.);
#697=FACE_OUTER_BOUND('',#918,.T.);
#914=EDGE_LOOP('',(#3035,#3036,#3037,#3038));
#915=EDGE_LOOP('',(#3039,#3040,#3041,#3042));
#916=EDGE_LOOP('',(#3043));
#917=EDGE_LOOP('',(#3044));
#918=EDGE_LOOP('',(#3045));
#919=EDGE_LOOP('',(#3046));
#1182=LINE('',#5743,#1442);
#1183=LINE('',#5749,#1443);
#1442=VECTOR('',#4699,0.32);
#1443=VECTOR('',#4706,0.6);
#1553=CIRCLE('',#3739,0.32);
#1554=CIRCLE('',#3740,0.32);
#1555=CIRCLE('',#3742,0.6);
#1556=CIRCLE('',#3743,0.6);
#1805=VERTEX_POINT('',#5740);
#1806=VERTEX_POINT('',#5742);
#1807=VERTEX_POINT('',#5746);
#1808=VERTEX_POINT('',#5748);
#2218=EDGE_CURVE('',#1805,#1805,#1553,.T.);
#2219=EDGE_CURVE('',#1805,#1806,#1182,.T.);
#2220=EDGE_CURVE('',#1806,#1806,#1554,.T.);
#2221=EDGE_CURVE('',#1807,#1807,#1555,.T.);
#2222=EDGE_CURVE('',#1807,#1808,#1183,.T.);
#2223=EDGE_CURVE('',#1808,#1808,#1556,.T.);
#3035=ORIENTED_EDGE('',*,*,#2218,.F.);
#3036=ORIENTED_EDGE('',*,*,#2219,.T.);
#3037=ORIENTED_EDGE('',*,*,#2220,.T.);
#3038=ORIENTED_EDGE('',*,*,#2219,.F.);
#3039=ORIENTED_EDGE('',*,*,#2221,.F.);
#3040=ORIENTED_EDGE('',*,*,#2222,.T.);
#3041=ORIENTED_EDGE('',*,*,#2223,.T.);
#3042=ORIENTED_EDGE('',*,*,#2222,.F.);
#3043=ORIENTED_EDGE('',*,*,#2221,.T.);
#3044=ORIENTED_EDGE('',*,*,#2218,.T.);
#3045=ORIENTED_EDGE('',*,*,#2223,.F.);
#3046=ORIENTED_EDGE('',*,*,#2220,.F.);
#3146=CYLINDRICAL_SURFACE('',#3738,0.32);
#3147=CYLINDRICAL_SURFACE('',#3741,0.6);
#3316=ADVANCED_FACE('',(#694),#3146,.F.);
#3317=ADVANCED_FACE('',(#695),#3147,.T.);
#3318=ADVANCED_FACE('',(#696,#401),#517,.T.);
#3319=ADVANCED_FACE('',(#697,#402),#518,.F.);
#3342=CLOSED_SHELL('',(#3316,#3317,#3318,#3319));
#3737=AXIS2_PLACEMENT_3D('',#5738,#4693,#4694);
#3738=AXIS2_PLACEMENT_3D('',#5739,#4695,#4696);
#3739=AXIS2_PLACEMENT_3D('',#5741,#4697,#4698);
#3740=AXIS2_PLACEMENT_3D('',#5744,#4700,#4701);
#3741=AXIS2_PLACEMENT_3D('',#5745,#4702,#4703);
#3742=AXIS2_PLACEMENT_3D('',#5747,#4704,#4705);
#3743=AXIS2_PLACEMENT_3D('',#5750,#4707,#4708);
#3744=AXIS2_PLACEMENT_3D('',#5751,#4709,#4710);
#3745=AXIS2_PLACEMENT_3D('',#5752,#4711,#4712);
#4693=DIRECTION('axis',(0.,0.,1.));
#4694=DIRECTION('refdir',(1.,0.,0.));
#4695=DIRECTION('center_axis',(0.,1.,0.));
#4696=DIRECTION('ref_axis',(1.,0.,0.));
#4697=DIRECTION('center_axis',(0.,-1.,0.));
#4698=DIRECTION('ref_axis',(1.,0.,0.));
#4699=DIRECTION('',(0.,-1.,0.));
#4700=DIRECTION('center_axis',(0.,-1.,0.));
#4701=DIRECTION('ref_axis',(1.,0.,0.));
#4702=DIRECTION('center_axis',(0.,1.,0.));
#4703=DIRECTION('ref_axis',(1.,0.,0.));
#4704=DIRECTION('center_axis',(0.,1.,0.));
#4705=DIRECTION('ref_axis',(1.,0.,0.));
#4706=DIRECTION('',(0.,-1.,0.));
#4707=DIRECTION('center_axis',(0.,1.,0.));
#4708=DIRECTION('ref_axis',(1.,0.,0.));
#4709=DIRECTION('center_axis',(0.,1.,0.));
#4710=DIRECTION('ref_axis',(1.,0.,0.));
#4711=DIRECTION('center_axis',(0.,1.,0.));
#4712=DIRECTION('ref_axis',(1.,0.,0.));
#5738=CARTESIAN_POINT('',(0.,0.,0.));
#5739=CARTESIAN_POINT('Origin',(0.,0.,0.));
#5740=CARTESIAN_POINT('',(-0.32,0.16,3.91886975727153E-17));
#5741=CARTESIAN_POINT('Origin',(0.,0.16,0.));
#5742=CARTESIAN_POINT('',(-0.32,0.,3.91886975727153E-17));
#5743=CARTESIAN_POINT('',(-0.32,0.,3.91886975727153E-17));
#5744=CARTESIAN_POINT('Origin',(0.,0.,0.));
#5745=CARTESIAN_POINT('Origin',(0.,0.,0.));
#5746=CARTESIAN_POINT('',(-0.6,0.16,7.34788079488412E-17));
#5747=CARTESIAN_POINT('Origin',(0.,0.16,0.));
#5748=CARTESIAN_POINT('',(-0.6,0.,7.34788079488412E-17));
#5749=CARTESIAN_POINT('',(-0.6,0.,7.34788079488412E-17));
#5750=CARTESIAN_POINT('Origin',(0.,0.,0.));
#5751=CARTESIAN_POINT('Origin',(0.,0.16,0.));
#5752=CARTESIAN_POINT('Origin',(0.,0.,0.));
#5903=UNCERTAINTY_MEASURE_WITH_UNIT(LENGTH_MEASURE(0.001),#5930,
'DISTANCE_ACCURACY_VALUE',
'Maximum model space distance between geometric entities at asserted c
onnectivities');
#5905=UNCERTAINTY_MEASURE_WITH_UNIT(LENGTH_MEASURE(0.001),#5930,
'DISTANCE_ACCURACY_VALUE',
'Maximum model space distance between geometric entities at asserted c
onnectivities');
#5927=(
GEOMETRIC_REPRESENTATION_CONTEXT(3)
GLOBAL_UNCERTAINTY_ASSIGNED_CONTEXT((#5903))
GLOBAL_UNIT_ASSIGNED_CONTEXT((#5930,#5932,#5933))
REPRESENTATION_CONTEXT('','3D')
);
#5929=(
GEOMETRIC_REPRESENTATION_CONTEXT(3)
GLOBAL_UNCERTAINTY_ASSIGNED_CONTEXT((#5905))
GLOBAL_UNIT_ASSIGNED_CONTEXT((#5930,#5932,#5933))
REPRESENTATION_CONTEXT('','3D')
);
#5930=(
LENGTH_UNIT()
NAMED_UNIT(*)
SI_UNIT(.CENTI.,.METRE.)
);
#5932=(
NAMED_UNIT(*)
PLANE_ANGLE_UNIT()
SI_UNIT($,.RADIAN.)
);
#5933=(
NAMED_UNIT(*)
SI_UNIT($,.STERADIAN.)
SOLID_ANGLE_UNIT()
);
#5955=SHAPE_DEFINITION_REPRESENTATION(#5985,#6060);
#5985=PRODUCT_DEFINITION_SHAPE('',$,#6084);
#6060=SHAPE_REPRESENTATION('',(#3737),#5927);
#6062=PRODUCT_DEFINITION_CONTEXT('part definition',#6133,'design');
#6084=PRODUCT_DEFINITION('Flat Washer - M6','Flat Washer - M6',#6107,
#6062);
#6107=PRODUCT_DEFINITION_FORMATION('',$,#6156);
#6133=APPLICATION_CONTEXT(
'Core Data for Automotive Mechanical Design Process');
#6134=PRODUCT_CONTEXT('part definition',#6133,'mechanical');
#6156=PRODUCT('Flat Washer - M6','Flat Washer - M6',
'Flat Washer - M6',(#6134));
#6221=COLOUR_RGB('Black',0.12,0.14,0.17);
#6222=FILL_AREA_STYLE_COLOUR('',#6221);
#6223=FILL_AREA_STYLE('',(#6222));
#6224=SURFACE_STYLE_FILL_AREA(#6223);
#6225=SURFACE_SIDE_STYLE('',(#6224));
#6226=SURFACE_STYLE_USAGE(.BOTH.,#6225);
#6227=PRESENTATION_STYLE_ASSIGNMENT((#6226));
ENDSEC;
END-ISO-10303-21;
